ISO-10303-21;
HEADER;
/* Generated by software containing ST-Developer
 * from STEP Tools, Inc. (www.steptools.com) 
 */

FILE_DESCRIPTION(
/* description */ ('PAT-054'),
/* implementation_level */ '2;1');

FILE_NAME(
/* name */ 'Flat Washer - M5 (1).step',
/* time_stamp */ '2026-10-29T16:38:13-07:00',
/* author */ (''),
/* organization */ (''),
/* preprocessor_version */ 'ST-DEVELOPER v20.2',
/* originating_system */ 'Autodesk Translation Framework v15.17.0.0',
/* authorisation */ '');

FILE_SCHEMA (('AUTOMOTIVE_DESIGN { 1 0 10303 214 3 1 1 }'));
ENDSEC;

DATA;
#10=MECHANICAL_DESIGN_GEOMETRIC_PRESENTATION_REPRESENTATION('',(#943),#33981);
#789=CONICAL_SURFACE('',#14390,0.275,0.785398163397449);
#840=SHAPE_REPRESENTATION_RELATIONSHIP('SRR','None',#34217,#884);
#884=ADVANCED_BREP_SHAPE_REPRESENTATION('',(#1001),#33965);
#943=STYLED_ITEM('',(#34524),#1001);
#1001=MANIFOLD_SOLID_BREP('Body1',#13055);
#1189=FACE_BOUND('',#2895,.T.);
#1190=FACE_BOUND('',#2898,.T.);
#1475=PLANE('',#14395);
#1476=PLANE('',#14399);
#1992=FACE_OUTER_BOUND('',#2892,.T.);
#1993=FACE_OUTER_BOUND('',#2893,.T.);
#1994=FACE_OUTER_BOUND('',#2894,.T.);
#1995=FACE_OUTER_BOUND('',#2896,.T.);
#1996=FACE_OUTER_BOUND('',#2897,.T.);
#2892=EDGE_LOOP('',(#10469,#10470,#10471,#10472));
#2893=EDGE_LOOP('',(#10473,#10474,#10475,#10476));
#2894=EDGE_LOOP('',(#10477));
#2895=EDGE_LOOP('',(#10478));
#2896=EDGE_LOOP('',(#10479,#10480,#10481,#10482));
#2897=EDGE_LOOP('',(#10483));
#2898=EDGE_LOOP('',(#10484));
#3830=LINE('',#21254,#4764);
#3831=LINE('',#21258,#4765);
#3832=LINE('',#21265,#4766);
#4764=VECTOR('',#17149,0.275);
#4765=VECTOR('',#17154,0.265);
#4766=VECTOR('',#17163,0.5);
#5468=CIRCLE('',#14391,0.285);
#5469=CIRCLE('',#14392,0.265);
#5470=CIRCLE('',#14394,0.265);
#5471=CIRCLE('',#14396,0.5);
#5472=CIRCLE('',#14398,0.5);
#6246=VERTEX_POINT('',#21251);
#6247=VERTEX_POINT('',#21253);
#6248=VERTEX_POINT('',#21257);
#6249=VERTEX_POINT('',#21261);
#6250=VERTEX_POINT('',#21264);
#7734=EDGE_CURVE('',#6246,#6246,#5468,.T.);
#7735=EDGE_CURVE('',#6246,#6247,#3830,.T.);
#7736=EDGE_CURVE('',#6247,#6247,#5469,.T.);
#7737=EDGE_CURVE('',#6247,#6248,#3831,.T.);
#7738=EDGE_CURVE('',#6248,#6248,#5470,.T.);
#7739=EDGE_CURVE('',#6249,#6249,#5471,.T.);
#7740=EDGE_CURVE('',#6249,#6250,#3832,.T.);
#7741=EDGE_CURVE('',#6250,#6250,#5472,.T.);
#10469=ORIENTED_EDGE('',*,*,#7734,.T.);
#10470=ORIENTED_EDGE('',*,*,#7735,.T.);
#10471=ORIENTED_EDGE('',*,*,#7736,.T.);
#10472=ORIENTED_EDGE('',*,*,#7735,.F.);
#10473=ORIENTED_EDGE('',*,*,#7736,.F.);
#10474=ORIENTED_EDGE('',*,*,#7737,.T.);
#10475=ORIENTED_EDGE('',*,*,#7738,.T.);
#10476=ORIENTED_EDGE('',*,*,#7737,.F.);
#10477=ORIENTED_EDGE('',*,*,#7739,.T.);
#10478=ORIENTED_EDGE('',*,*,#7734,.F.);
#10479=ORIENTED_EDGE('',*,*,#7739,.F.);
#10480=ORIENTED_EDGE('',*,*,#7740,.T.);
#10481=ORIENTED_EDGE('',*,*,#7741,.T.);
#10482=ORIENTED_EDGE('',*,*,#7740,.F.);
#10483=ORIENTED_EDGE('',*,*,#7741,.F.);
#10484=ORIENTED_EDGE('',*,*,#7738,.F.);
#12103=CYLINDRICAL_SURFACE('',#14393,0.265);
#12104=CYLINDRICAL_SURFACE('',#14397,0.5);
#12704=ADVANCED_FACE('',(#1992),#789,.F.);
#12705=ADVANCED_FACE('',(#1993),#12103,.F.);
#12706=ADVANCED_FACE('',(#1994,#1189),#1475,.T.);
#12707=ADVANCED_FACE('',(#1995),#12104,.T.);
#12708=ADVANCED_FACE('',(#1996,#1190),#1476,.F.);
#13055=CLOSED_SHELL('',(#12704,#12705,#12706,#12707,#12708));
#14389=AXIS2_PLACEMENT_3D('',#21249,#17143,#17144);
#14390=AXIS2_PLACEMENT_3D('',#21250,#17145,#17146);
#14391=AXIS2_PLACEMENT_3D('',#21252,#17147,#17148);
#14392=AXIS2_PLACEMENT_3D('',#21255,#17150,#17151);
#14393=AXIS2_PLACEMENT_3D('',#21256,#17152,#17153);
#14394=AXIS2_PLACEMENT_3D('',#21259,#17155,#17156);
#14395=AXIS2_PLACEMENT_3D('',#21260,#17157,#17158);
#14396=AXIS2_PLACEMENT_3D('',#21262,#17159,#17160);
#14397=AXIS2_PLACEMENT_3D('',#21263,#17161,#17162);
#14398=AXIS2_PLACEMENT_3D('',#21266,#17164,#17165);
#14399=AXIS2_PLACEMENT_3D('',#21267,#17166,#17167);
#17143=DIRECTION('axis',(0.,0.,1.));
#17144=DIRECTION('refdir',(1.,0.,0.));
#17145=DIRECTION('center_axis',(0.,1.,0.));
#17146=DIRECTION('ref_axis',(1.,0.,0.));
#17147=DIRECTION('center_axis',(0.,1.,0.));
#17148=DIRECTION('ref_axis',(1.,0.,0.));
#17149=DIRECTION('',(0.707106781186548,-0.707106781186547,-8.65956056235494E-17));
#17150=DIRECTION('center_axis',(0.,-1.,0.));
#17151=DIRECTION('ref_axis',(1.,0.,0.));
#17152=DIRECTION('center_axis',(0.,1.,0.));
#17153=DIRECTION('ref_axis',(1.,0.,0.));
#17154=DIRECTION('',(0.,-1.,0.));
#17155=DIRECTION('center_axis',(0.,-1.,0.));
#17156=DIRECTION('ref_axis',(1.,0.,0.));
#17157=DIRECTION('center_axis',(0.,1.,0.));
#17158=DIRECTION('ref_axis',(1.,0.,0.));
#17159=DIRECTION('center_axis',(0.,1.,0.));
#17160=DIRECTION('ref_axis',(1.,0.,0.));
#17161=DIRECTION('center_axis',(0.,1.,0.));
#17162=DIRECTION('ref_axis',(1.,0.,0.));
#17163=DIRECTION('',(0.,-1.,0.));
#17164=DIRECTION('center_axis',(0.,1.,0.));
#17165=DIRECTION('ref_axis',(1.,0.,0.));
#17166=DIRECTION('center_axis',(0.,1.,0.));
#17167=DIRECTION('ref_axis',(1.,0.,0.));
#21249=CARTESIAN_POINT('',(0.,0.,0.));
#21250=CARTESIAN_POINT('Origin',(0.,0.09,0.));
#21251=CARTESIAN_POINT('',(-0.285,0.1,3.49024337756996E-17));
#21252=CARTESIAN_POINT('Origin',(0.,0.1,0.));
#21253=CARTESIAN_POINT('',(-0.265,0.08,-3.24531401774049E-17));
#21254=CARTESIAN_POINT('',(-0.275,0.09,3.36777869765522E-17));
#21255=CARTESIAN_POINT('Origin',(0.,0.08,0.));
#21256=CARTESIAN_POINT('Origin',(0.,0.,0.));
#21257=CARTESIAN_POINT('',(-0.265,0.,3.24531401774049E-17));
#21258=CARTESIAN_POINT('',(-0.265,0.,3.24531401774049E-17));
#21259=CARTESIAN_POINT('Origin',(0.,0.,0.));
#21260=CARTESIAN_POINT('Origin',(0.,0.1,0.));
#21261=CARTESIAN_POINT('',(-0.5,0.1,6.12323399573677E-17));
#21262=CARTESIAN_POINT('Origin',(0.,0.1,0.));
#21263=CARTESIAN_POINT('Origin',(0.,0.,0.));
#21264=CARTESIAN_POINT('',(-0.5,0.,6.12323399573677E-17));
#21265=CARTESIAN_POINT('',(-0.5,0.,6.12323399573677E-17));
#21266=CARTESIAN_POINT('Origin',(0.,0.,0.));
#21267=CARTESIAN_POINT('Origin',(0.,0.,0.));
#33913=UNCERTAINTY_MEASURE_WITH_UNIT(LENGTH_MEASURE(0.001),#33982,
'DISTANCE_ACCURACY_VALUE',
'Maximum model space distance between geometric entities at asserted c
onnectivities');
#33929=UNCERTAINTY_MEASURE_WITH_UNIT(LENGTH_MEASURE(0.001),#33982,
'DISTANCE_ACCURACY_VALUE',
'Maximum model space distance between geometric entities at asserted c
onnectivities');
#33965=(
GEOMETRIC_REPRESENTATION_CONTEXT(3)
GLOBAL_UNCERTAINTY_ASSIGNED_CONTEXT((#33913))
GLOBAL_UNIT_ASSIGNED_CONTEXT((#33982,#33984,#33985))
REPRESENTATION_CONTEXT('','3D')
);
#33981=(
GEOMETRIC_REPRESENTATION_CONTEXT(3)
GLOBAL_UNCERTAINTY_ASSIGNED_CONTEXT((#33929))
GLOBAL_UNIT_ASSIGNED_CONTEXT((#33982,#33984,#33985))
REPRESENTATION_CONTEXT('','3D')
);
#33982=(
LENGTH_UNIT()
NAMED_UNIT(*)
SI_UNIT(.CENTI.,.METRE.)
);
#33984=(
NAMED_UNIT(*)
PLANE_ANGLE_UNIT()
SI_UNIT($,.RADIAN.)
);
#33985=(
NAMED_UNIT(*)
SI_UNIT($,.STERADIAN.)
SOLID_ANGLE_UNIT()
);
#34021=SHAPE_DEFINITION_REPRESENTATION(#34085,#34217);
#34085=PRODUCT_DEFINITION_SHAPE('',$,#34269);
#34217=SHAPE_REPRESENTATION('',(#14389),#33965);
#34233=PRODUCT_DEFINITION_CONTEXT('part definition',#34388,'design');
#34269=PRODUCT_DEFINITION('Flat Washer - M5 (1)','Flat Washer - M5 (1)',#34320,
#34233);
#34320=PRODUCT_DEFINITION_FORMATION('',$,#34425);
#34388=APPLICATION_CONTEXT(
'Core Data for Automotive Mechanical Design Process');
#34389=PRODUCT_CONTEXT('part definition',#34388,'mechanical');
#34425=PRODUCT('Flat Washer - M5 (1)','Flat Washer - M5 (1)',
'Flat Washer - M5 (1)',(#34389));
#34518=COLOUR_RGB('Black',0.12,0.14,0.17);
#34519=FILL_AREA_STYLE_COLOUR('',#34518);
#34520=FILL_AREA_STYLE('',(#34519));
#34521=SURFACE_STYLE_FILL_AREA(#34520);
#34522=SURFACE_SIDE_STYLE('',(#34521));
#34523=SURFACE_STYLE_USAGE(.BOTH.,#34522);
#34524=PRESENTATION_STYLE_ASSIGNMENT((#34523));
ENDSEC;
END-ISO-10303-21;
